ISO-10303-21;
HEADER;
/* Generated by software containing ST-Developer
 * from STEP Tools, Inc. (www.steptools.com) 
 */

FILE_DESCRIPTION(
/* description */ ('Door-style hinge test fixture with detent'),
/* implementation_level */ '2;1');

FILE_NAME(
/* name */ 'Pin end keeper (1).step',
/* time_stamp */ '2026-10-28T03:24:57-07:00',
/* author */ (''),
/* organization */ (''),
/* preprocessor_version */ 'ST-DEVELOPER v20.2',
/* originating_system */ 'Autodesk Translation Framework v15.17.0.0',
/* authorisation */ '');

FILE_SCHEMA (('AUTOMOTIVE_DESIGN { 1 0 10303 214 3 1 1 }'));
ENDSEC;

DATA;
#10=MECHANICAL_DESIGN_GEOMETRIC_PRESENTATION_REPRESENTATION('',(#360),#9813);
#289=SHAPE_REPRESENTATION_RELATIONSHIP('SRR','None',#9968,#320);
#320=ADVANCED_BREP_SHAPE_REPRESENTATION('',(#398),#9811);
#360=STYLED_ITEM('',(#10183),#398);
#398=MANIFOLD_SOLID_BREP('Body1',#4793);
#497=FACE_BOUND('',#1313,.T.);
#498=FACE_BOUND('',#1315,.T.);
#650=PLANE('',#5714);
#651=PLANE('',#5715);
#927=FACE_OUTER_BOUND('',#1310,.T.);
#928=FACE_OUTER_BOUND('',#1311,.T.);
#929=FACE_OUTER_BOUND('',#1312,.T.);
#930=FACE_OUTER_BOUND('',#1314,.T.);
#1310=EDGE_LOOP('',(#4305,#4306,#4307,#4308));
#1311=EDGE_LOOP('',(#4309,#4310,#4311,#4312));
#1312=EDGE_LOOP('',(#4313));
#1313=EDGE_LOOP('',(#4314));
#1314=EDGE_LOOP('',(#4315));
#1315=EDGE_LOOP('',(#4316));
#1628=LINE('',#9653,#1948);
#1629=LINE('',#9659,#1949);
#1948=VECTOR('',#7189,0.225);
#1949=VECTOR('',#7196,0.9);
#2209=CIRCLE('',#5709,0.225);
#2210=CIRCLE('',#5710,0.225);
#2211=CIRCLE('',#5712,0.9);
#2212=CIRCLE('',#5713,0.9);
#2596=VERTEX_POINT('',#9650);
#2597=VERTEX_POINT('',#9652);
#2598=VERTEX_POINT('',#9656);
#2599=VERTEX_POINT('',#9658);
#3169=EDGE_CURVE('',#2596,#2596,#2209,.T.);
#3170=EDGE_CURVE('',#2596,#2597,#1628,.T.);
#3171=EDGE_CURVE('',#2597,#2597,#2210,.T.);
#3172=EDGE_CURVE('',#2598,#2598,#2211,.T.);
#3173=EDGE_CURVE('',#2598,#2599,#1629,.T.);
#3174=EDGE_CURVE('',#2599,#2599,#2212,.T.);
#4305=ORIENTED_EDGE('',*,*,#3169,.F.);
#4306=ORIENTED_EDGE('',*,*,#3170,.T.);
#4307=ORIENTED_EDGE('',*,*,#3171,.T.);
#4308=ORIENTED_EDGE('',*,*,#3170,.F.);
#4309=ORIENTED_EDGE('',*,*,#3172,.F.);
#4310=ORIENTED_EDGE('',*,*,#3173,.T.);
#4311=ORIENTED_EDGE('',*,*,#3174,.T.);
#4312=ORIENTED_EDGE('',*,*,#3173,.F.);
#4313=ORIENTED_EDGE('',*,*,#3172,.T.);
#4314=ORIENTED_EDGE('',*,*,#3169,.T.);
#4315=ORIENTED_EDGE('',*,*,#3174,.F.);
#4316=ORIENTED_EDGE('',*,*,#3171,.F.);
#4464=CYLINDRICAL_SURFACE('',#5708,0.225);
#4465=CYLINDRICAL_SURFACE('',#5711,0.9);
#4732=ADVANCED_FACE('',(#927),#4464,.F.);
#4733=ADVANCED_FACE('',(#928),#4465,.T.);
#4734=ADVANCED_FACE('',(#929,#497),#650,.T.);
#4735=ADVANCED_FACE('',(#930,#498),#651,.F.);
#4793=CLOSED_SHELL('',(#4732,#4733,#4734,#4735));
#5707=AXIS2_PLACEMENT_3D('',#9648,#7183,#7184);
#5708=AXIS2_PLACEMENT_3D('',#9649,#7185,#7186);
#5709=AXIS2_PLACEMENT_3D('',#9651,#7187,#7188);
#5710=AXIS2_PLACEMENT_3D('',#9654,#7190,#7191);
#5711=AXIS2_PLACEMENT_3D('',#9655,#7192,#7193);
#5712=AXIS2_PLACEMENT_3D('',#9657,#7194,#7195);
#5713=AXIS2_PLACEMENT_3D('',#9660,#7197,#7198);
#5714=AXIS2_PLACEMENT_3D('',#9661,#7199,#7200);
#5715=AXIS2_PLACEMENT_3D('',#9662,#7201,#7202);
#7183=DIRECTION('axis',(0.,0.,1.));
#7184=DIRECTION('refdir',(1.,0.,0.));
#7185=DIRECTION('center_axis',(0.,0.,1.));
#7186=DIRECTION('ref_axis',(1.,0.,0.));
#7187=DIRECTION('center_axis',(0.,0.,-1.));
#7188=DIRECTION('ref_axis',(1.,0.,0.));
#7189=DIRECTION('',(0.,0.,-1.));
#7190=DIRECTION('center_axis',(0.,0.,-1.));
#7191=DIRECTION('ref_axis',(1.,0.,0.));
#7192=DIRECTION('center_axis',(0.,0.,1.));
#7193=DIRECTION('ref_axis',(1.,0.,0.));
#7194=DIRECTION('center_axis',(0.,0.,1.));
#7195=DIRECTION('ref_axis',(1.,0.,0.));
#7196=DIRECTION('',(0.,0.,-1.));
#7197=DIRECTION('center_axis',(0.,0.,1.));
#7198=DIRECTION('ref_axis',(1.,0.,0.));
#7199=DIRECTION('center_axis',(0.,0.,1.));
#7200=DIRECTION('ref_axis',(1.,0.,0.));
#7201=DIRECTION('center_axis',(0.,0.,1.));
#7202=DIRECTION('ref_axis',(1.,0.,0.));
#9648=CARTESIAN_POINT('',(0.,0.,0.));
#9649=CARTESIAN_POINT('Origin',(0.,0.,12.));
#9650=CARTESIAN_POINT('',(-0.225,-2.75545529808154E-17,12.2));
#9651=CARTESIAN_POINT('Origin',(0.,0.,12.2));
#9652=CARTESIAN_POINT('',(-0.225,-2.75545529808154E-17,12.));
#9653=CARTESIAN_POINT('',(-0.225,-2.75545529808154E-17,12.));
#9654=CARTESIAN_POINT('Origin',(0.,0.,12.));
#9655=CARTESIAN_POINT('Origin',(0.,0.,12.));
#9656=CARTESIAN_POINT('',(-0.9,-1.10218211923262E-16,12.2));
#9657=CARTESIAN_POINT('Origin',(0.,0.,12.2));
#9658=CARTESIAN_POINT('',(-0.9,-1.10218211923262E-16,12.));
#9659=CARTESIAN_POINT('',(-0.9,-1.10218211923262E-16,12.));
#9660=CARTESIAN_POINT('Origin',(0.,0.,12.));
#9661=CARTESIAN_POINT('Origin',(0.,0.,12.2));
#9662=CARTESIAN_POINT('Origin',(0.,0.,12.));
#9775=UNCERTAINTY_MEASURE_WITH_UNIT(LENGTH_MEASURE(0.001),#9814,
'DISTANCE_ACCURACY_VALUE',
'Maximum model space distance between geometric entities at asserted c
onnectivities');
#9777=UNCERTAINTY_MEASURE_WITH_UNIT(LENGTH_MEASURE(0.001),#9814,
'DISTANCE_ACCURACY_VALUE',
'Maximum model space distance between geometric entities at asserted c
onnectivities');
#9811=(
GEOMETRIC_REPRESENTATION_CONTEXT(3)
GLOBAL_UNCERTAINTY_ASSIGNED_CONTEXT((#9775))
GLOBAL_UNIT_ASSIGNED_CONTEXT((#9814,#9816,#9817))
REPRESENTATION_CONTEXT('','3D')
);
#9813=(
GEOMETRIC_REPRESENTATION_CONTEXT(3)
GLOBAL_UNCERTAINTY_ASSIGNED_CONTEXT((#9777))
GLOBAL_UNIT_ASSIGNED_CONTEXT((#9814,#9816,#9817))
REPRESENTATION_CONTEXT('','3D')
);
#9814=(
LENGTH_UNIT()
NAMED_UNIT(*)
SI_UNIT(.CENTI.,.METRE.)
);
#9816=(
NAMED_UNIT(*)
PLANE_ANGLE_UNIT()
SI_UNIT($,.RADIAN.)
);
#9817=(
NAMED_UNIT(*)
SI_UNIT($,.STERADIAN.)
SOLID_ANGLE_UNIT()
);
#9851=SHAPE_DEFINITION_REPRESENTATION(#9924,#9968);
#9924=PRODUCT_DEFINITION_SHAPE('',$,#10004);
#9968=SHAPE_REPRESENTATION('',(#5707),#9811);
#9970=PRODUCT_DEFINITION_CONTEXT('part definition',#10077,'design');
#10004=PRODUCT_DEFINITION('Pin end keeper (1)','Pin end keeper (1)',#10039,
#9970);
#10039=PRODUCT_DEFINITION_FORMATION('',$,#10112);
#10077=APPLICATION_CONTEXT(
'Core Data for Automotive Mechanical Design Process');
#10078=PRODUCT_CONTEXT('part definition',#10077,'mechanical');
#10112=PRODUCT('Pin end keeper (1)','Pin end keeper (1)','Pin end keeper (1)',
(#10078));
#10177=COLOUR_RGB('Grey',0.48,0.52,0.57);
#10178=FILL_AREA_STYLE_COLOUR('',#10177);
#10179=FILL_AREA_STYLE('',(#10178));
#10180=SURFACE_STYLE_FILL_AREA(#10179);
#10181=SURFACE_SIDE_STYLE('',(#10180));
#10182=SURFACE_STYLE_USAGE(.BOTH.,#10181);
#10183=PRESENTATION_STYLE_ASSIGNMENT((#10182));
ENDSEC;
END-ISO-10303-21;
